ISO-10303-21;
HEADER;
/* Generated by software containing ST-Developer
 * from STEP Tools, Inc. (www.steptools.com) 
 */

FILE_DESCRIPTION(
/* description */ ('PAT-083'),
/* implementation_level */ '2;1');

FILE_NAME(
/* name */ 'Hex Nut - M8.step',
/* time_stamp */ '2026-10-29T20:18:00-07:00',
/* author */ (''),
/* organization */ (''),
/* preprocessor_version */ 'ST-DEVELOPER v20.2',
/* originating_system */ 'Autodesk Translation Framework v15.17.0.0',
/* authorisation */ '');

FILE_SCHEMA (('AUTOMOTIVE_DESIGN { 1 0 10303 214 3 1 1 }'));
ENDSEC;

DATA;
#10=MECHANICAL_DESIGN_GEOMETRIC_PRESENTATION_REPRESENTATION('',(#251),#8428);
#135=(
BOUNDED_CURVE()
B_SPLINE_CURVE(2,(#8219,#8220,#8221),.UNSPECIFIED.,.F.,.F.)
B_SPLINE_CURVE_WITH_KNOTS((3,3),(0.14973948338295,0.97160236658079),
 .UNSPECIFIED.)
CURVE()
GEOMETRIC_REPRESENTATION_ITEM()
RATIONAL_B_SPLINE_CURVE((1.07140024848292,1.23714644374248,1.07140024848292))
REPRESENTATION_ITEM('')
);
#136=(
BOUNDED_CURVE()
B_SPLINE_CURVE(2,(#8223,#8224,#8225),.UNSPECIFIED.,.F.,.F.)
B_SPLINE_CURVE_WITH_KNOTS((3,3),(0.14973948338295,0.971602366580789),
 .UNSPECIFIED.)
CURVE()
GEOMETRIC_REPRESENTATION_ITEM()
RATIONAL_B_SPLINE_CURVE((1.07140024848292,1.23714644374248,1.07140024848292))
REPRESENTATION_ITEM('')
);
#137=(
BOUNDED_CURVE()
B_SPLINE_CURVE(2,(#8230,#8231,#8232),.UNSPECIFIED.,.F.,.F.)
B_SPLINE_CURVE_WITH_KNOTS((3,3),(0.14973948338295,0.97160236658079),
 .UNSPECIFIED.)
CURVE()
GEOMETRIC_REPRESENTATION_ITEM()
RATIONAL_B_SPLINE_CURVE((1.07140024848292,1.23714644374248,1.07140024848292))
REPRESENTATION_ITEM('')
);
#138=(
BOUNDED_CURVE()
B_SPLINE_CURVE(2,(#8234,#8235,#8236),.UNSPECIFIED.,.F.,.F.)
B_SPLINE_CURVE_WITH_KNOTS((3,3),(0.14973948338295,0.97160236658079),
 .UNSPECIFIED.)
CURVE()
GEOMETRIC_REPRESENTATION_ITEM()
RATIONAL_B_SPLINE_CURVE((1.07140024848292,1.23714644374248,1.07140024848292))
REPRESENTATION_ITEM('')
);
#139=(
BOUNDED_CURVE()
B_SPLINE_CURVE(2,(#8238,#8239,#8240),.UNSPECIFIED.,.F.,.F.)
B_SPLINE_CURVE_WITH_KNOTS((3,3),(0.14973948338295,0.971602366580789),
 .UNSPECIFIED.)
CURVE()
GEOMETRIC_REPRESENTATION_ITEM()
RATIONAL_B_SPLINE_CURVE((1.07140024848292,1.23714644374248,1.07140024848292))
REPRESENTATION_ITEM('')
);
#140=(
BOUNDED_CURVE()
B_SPLINE_CURVE(2,(#8241,#8242,#8243),.UNSPECIFIED.,.F.,.F.)
B_SPLINE_CURVE_WITH_KNOTS((3,3),(0.14973948338295,0.97160236658079),
 .UNSPECIFIED.)
CURVE()
GEOMETRIC_REPRESENTATION_ITEM()
RATIONAL_B_SPLINE_CURVE((1.07140024848292,1.23714644374248,1.07140024848292))
REPRESENTATION_ITEM('')
);
#141=(
BOUNDED_CURVE()
B_SPLINE_CURVE(2,(#8250,#8251,#8252),.UNSPECIFIED.,.F.,.F.)
B_SPLINE_CURVE_WITH_KNOTS((3,3),(0.14973948338295,0.97160236658079),
 .UNSPECIFIED.)
CURVE()
GEOMETRIC_REPRESENTATION_ITEM()
RATIONAL_B_SPLINE_CURVE((1.07140024848292,1.23714644374248,1.07140024848292))
REPRESENTATION_ITEM('')
);
#142=(
BOUNDED_CURVE()
B_SPLINE_CURVE(2,(#8254,#8255,#8256),.UNSPECIFIED.,.F.,.F.)
B_SPLINE_CURVE_WITH_KNOTS((3,3),(0.14973948338295,0.97160236658079),
 .UNSPECIFIED.)
CURVE()
GEOMETRIC_REPRESENTATION_ITEM()
RATIONAL_B_SPLINE_CURVE((1.07140024848292,1.23714644374248,1.07140024848292))
REPRESENTATION_ITEM('')
);
#143=(
BOUNDED_CURVE()
B_SPLINE_CURVE(2,(#8258,#8259,#8260),.UNSPECIFIED.,.F.,.F.)
B_SPLINE_CURVE_WITH_KNOTS((3,3),(0.14973948338295,0.971602366580789),
 .UNSPECIFIED.)
CURVE()
GEOMETRIC_REPRESENTATION_ITEM()
RATIONAL_B_SPLINE_CURVE((1.07140024848292,1.23714644374248,1.07140024848292))
REPRESENTATION_ITEM('')
);
#144=(
BOUNDED_CURVE()
B_SPLINE_CURVE(2,(#8262,#8263,#8264),.UNSPECIFIED.,.F.,.F.)
B_SPLINE_CURVE_WITH_KNOTS((3,3),(0.14973948338295,0.97160236658079),
 .UNSPECIFIED.)
CURVE()
GEOMETRIC_REPRESENTATION_ITEM()
RATIONAL_B_SPLINE_CURVE((1.07140024848292,1.23714644374248,1.07140024848292))
REPRESENTATION_ITEM('')
);
#145=(
BOUNDED_CURVE()
B_SPLINE_CURVE(2,(#8266,#8267,#8268),.UNSPECIFIED.,.F.,.F.)
B_SPLINE_CURVE_WITH_KNOTS((3,3),(0.14973948338295,0.97160236658079),
 .UNSPECIFIED.)
CURVE()
GEOMETRIC_REPRESENTATION_ITEM()
RATIONAL_B_SPLINE_CURVE((1.07140024848292,1.23714644374248,1.07140024848292))
REPRESENTATION_ITEM('')
);
#146=(
BOUNDED_CURVE()
B_SPLINE_CURVE(2,(#8269,#8270,#8271),.UNSPECIFIED.,.F.,.F.)
B_SPLINE_CURVE_WITH_KNOTS((3,3),(0.14973948338295,0.971602366580789),
 .UNSPECIFIED.)
CURVE()
GEOMETRIC_REPRESENTATION_ITEM()
RATIONAL_B_SPLINE_CURVE((1.07140024848292,1.23714644374248,1.07140024848292))
REPRESENTATION_ITEM('')
);
#159=CONICAL_SURFACE('',#4373,0.734027674973257,1.0471975511966);
#160=CONICAL_SURFACE('',#4375,0.734027674973257,1.0471975511966);
#203=SHAPE_REPRESENTATION_RELATIONSHIP('SRR','None',#8537,#227);
#227=ADVANCED_BREP_SHAPE_REPRESENTATION('',(#273),#8426);
#251=STYLED_ITEM('',(#8712),#273);
#273=MANIFOLD_SOLID_BREP('Body1',#3699);
#353=FACE_BOUND('',#1026,.T.);
#354=FACE_BOUND('',#1028,.T.);
#478=PLANE('',#4377);
#479=PLANE('',#4378);
#480=PLANE('',#4379);
#481=PLANE('',#4383);
#482=PLANE('',#4384);
#483=PLANE('',#4385);
#484=PLANE('',#4386);
#485=PLANE('',#4387);
#705=FACE_OUTER_BOUND('',#1016,.T.);
#706=FACE_OUTER_BOUND('',#1017,.T.);
#707=FACE_OUTER_BOUND('',#1018,.T.);
#708=FACE_OUTER_BOUND('',#1019,.T.);
#709=FACE_OUTER_BOUND('',#1020,.T.);
#710=FACE_OUTER_BOUND('',#1021,.T.);
#711=FACE_OUTER_BOUND('',#1022,.T.);
#712=FACE_OUTER_BOUND('',#1023,.T.);
#713=FACE_OUTER_BOUND('',#1024,.T.);
#714=FACE_OUTER_BOUND('',#1025,.T.);
#715=FACE_OUTER_BOUND('',#1027,.T.);
#1016=EDGE_LOOP('',(#3264,#3265,#3266,#3267,#3268,#3269,#3270,#3271,#3272));
#1017=EDGE_LOOP('',(#3273,#3274,#3275,#3276,#3277,#3278,#3279,#3280,#3281));
#1018=EDGE_LOOP('',(#3282,#3283,#3284,#3285));
#1019=EDGE_LOOP('',(#3286,#3287,#3288,#3289));
#1020=EDGE_LOOP('',(#3290,#3291,#3292,#3293));
#1021=EDGE_LOOP('',(#3294,#3295,#3296,#3297));
#1022=EDGE_LOOP('',(#3298,#3299,#3300,#3301));
#1023=EDGE_LOOP('',(#3302,#3303,#3304,#3305));
#1024=EDGE_LOOP('',(#3306,#3307,#3308,#3309));
#1025=EDGE_LOOP('',(#3310));
#1026=EDGE_LOOP('',(#3311));
#1027=EDGE_LOOP('',(#3312));
#1028=EDGE_LOOP('',(#3313));
#1256=LINE('',#8227,#1500);
#1257=LINE('',#8248,#1501);
#1258=LINE('',#8273,#1502);
#1259=LINE('',#8274,#1503);
#1260=LINE('',#8276,#1504);
#1261=LINE('',#8278,#1505);
#1262=LINE('',#8283,#1506);
#1263=LINE('',#8286,#1507);
#1264=LINE('',#8288,#1508);
#1500=VECTOR('',#5466,0.734027674973257);
#1501=VECTOR('',#5473,0.734027674973257);
#1502=VECTOR('',#5476,1.);
#1503=VECTOR('',#5477,1.);
#1504=VECTOR('',#5480,1.);
#1505=VECTOR('',#5483,1.);
#1506=VECTOR('',#5488,0.4);
#1507=VECTOR('',#5493,1.);
#1508=VECTOR('',#5496,1.);
#1705=CIRCLE('',#4374,0.6175);
#1706=CIRCLE('',#4376,0.6175);
#1707=CIRCLE('',#4381,0.338975);
#1708=CIRCLE('',#4382,0.338975);
#1973=VERTEX_POINT('',#8217);
#1974=VERTEX_POINT('',#8218);
#1975=VERTEX_POINT('',#8222);
#1976=VERTEX_POINT('',#8226);
#1977=VERTEX_POINT('',#8229);
#1978=VERTEX_POINT('',#8233);
#1979=VERTEX_POINT('',#8237);
#1980=VERTEX_POINT('',#8245);
#1981=VERTEX_POINT('',#8247);
#1982=VERTEX_POINT('',#8249);
#1983=VERTEX_POINT('',#8253);
#1984=VERTEX_POINT('',#8257);
#1985=VERTEX_POINT('',#8261);
#1986=VERTEX_POINT('',#8265);
#1987=VERTEX_POINT('',#8280);
#1988=VERTEX_POINT('',#8282);
#2408=EDGE_CURVE('',#1973,#1974,#135,.T.);
#2409=EDGE_CURVE('',#1975,#1973,#136,.T.);
#2410=EDGE_CURVE('',#1975,#1976,#1256,.T.);
#2411=EDGE_CURVE('',#1976,#1976,#1705,.T.);
#2412=EDGE_CURVE('',#1977,#1975,#137,.T.);
#2413=EDGE_CURVE('',#1978,#1977,#138,.T.);
#2414=EDGE_CURVE('',#1979,#1978,#139,.T.);
#2415=EDGE_CURVE('',#1974,#1979,#140,.T.);
#2416=EDGE_CURVE('',#1980,#1980,#1706,.T.);
#2417=EDGE_CURVE('',#1980,#1981,#1257,.T.);
#2418=EDGE_CURVE('',#1982,#1981,#141,.T.);
#2419=EDGE_CURVE('',#1983,#1982,#142,.T.);
#2420=EDGE_CURVE('',#1984,#1983,#143,.T.);
#2421=EDGE_CURVE('',#1985,#1984,#144,.T.);
#2422=EDGE_CURVE('',#1986,#1985,#145,.T.);
#2423=EDGE_CURVE('',#1981,#1986,#146,.T.);
#2424=EDGE_CURVE('',#1977,#1986,#1258,.T.);
#2425=EDGE_CURVE('',#1978,#1985,#1259,.T.);
#2426=EDGE_CURVE('',#1975,#1981,#1260,.T.);
#2427=EDGE_CURVE('',#1973,#1982,#1261,.T.);
#2428=EDGE_CURVE('',#1987,#1987,#1707,.F.);
#2429=EDGE_CURVE('',#1987,#1988,#1262,.T.);
#2430=EDGE_CURVE('',#1988,#1988,#1708,.F.);
#2431=EDGE_CURVE('',#1974,#1983,#1263,.T.);
#2432=EDGE_CURVE('',#1979,#1984,#1264,.T.);
#3264=ORIENTED_EDGE('',*,*,#2408,.F.);
#3265=ORIENTED_EDGE('',*,*,#2409,.F.);
#3266=ORIENTED_EDGE('',*,*,#2410,.T.);
#3267=ORIENTED_EDGE('',*,*,#2411,.F.);
#3268=ORIENTED_EDGE('',*,*,#2410,.F.);
#3269=ORIENTED_EDGE('',*,*,#2412,.F.);
#3270=ORIENTED_EDGE('',*,*,#2413,.F.);
#3271=ORIENTED_EDGE('',*,*,#2414,.F.);
#3272=ORIENTED_EDGE('',*,*,#2415,.F.);
#3273=ORIENTED_EDGE('',*,*,#2416,.F.);
#3274=ORIENTED_EDGE('',*,*,#2417,.T.);
#3275=ORIENTED_EDGE('',*,*,#2418,.F.);
#3276=ORIENTED_EDGE('',*,*,#2419,.F.);
#3277=ORIENTED_EDGE('',*,*,#2420,.F.);
#3278=ORIENTED_EDGE('',*,*,#2421,.F.);
#3279=ORIENTED_EDGE('',*,*,#2422,.F.);
#3280=ORIENTED_EDGE('',*,*,#2423,.F.);
#3281=ORIENTED_EDGE('',*,*,#2417,.F.);
#3282=ORIENTED_EDGE('',*,*,#2413,.T.);
#3283=ORIENTED_EDGE('',*,*,#2424,.T.);
#3284=ORIENTED_EDGE('',*,*,#2422,.T.);
#3285=ORIENTED_EDGE('',*,*,#2425,.F.);
#3286=ORIENTED_EDGE('',*,*,#2412,.T.);
#3287=ORIENTED_EDGE('',*,*,#2426,.T.);
#3288=ORIENTED_EDGE('',*,*,#2423,.T.);
#3289=ORIENTED_EDGE('',*,*,#2424,.F.);
#3290=ORIENTED_EDGE('',*,*,#2409,.T.);
#3291=ORIENTED_EDGE('',*,*,#2427,.T.);
#3292=ORIENTED_EDGE('',*,*,#2418,.T.);
#3293=ORIENTED_EDGE('',*,*,#2426,.F.);
#3294=ORIENTED_EDGE('',*,*,#2428,.F.);
#3295=ORIENTED_EDGE('',*,*,#2429,.T.);
#3296=ORIENTED_EDGE('',*,*,#2430,.T.);
#3297=ORIENTED_EDGE('',*,*,#2429,.F.);
#3298=ORIENTED_EDGE('',*,*,#2408,.T.);
#3299=ORIENTED_EDGE('',*,*,#2431,.T.);
#3300=ORIENTED_EDGE('',*,*,#2419,.T.);
#3301=ORIENTED_EDGE('',*,*,#2427,.F.);
#3302=ORIENTED_EDGE('',*,*,#2414,.T.);
#3303=ORIENTED_EDGE('',*,*,#2425,.T.);
#3304=ORIENTED_EDGE('',*,*,#2421,.T.);
#3305=ORIENTED_EDGE('',*,*,#2432,.F.);
#3306=ORIENTED_EDGE('',*,*,#2415,.T.);
#3307=ORIENTED_EDGE('',*,*,#2432,.T.);
#3308=ORIENTED_EDGE('',*,*,#2420,.T.);
#3309=ORIENTED_EDGE('',*,*,#2431,.F.);
#3310=ORIENTED_EDGE('',*,*,#2416,.T.);
#3311=ORIENTED_EDGE('',*,*,#2428,.T.);
#3312=ORIENTED_EDGE('',*,*,#2411,.T.);
#3313=ORIENTED_EDGE('',*,*,#2430,.F.);
#3440=CYLINDRICAL_SURFACE('',#4380,0.338975);
#3652=ADVANCED_FACE('',(#705),#159,.T.);
#3653=ADVANCED_FACE('',(#706),#160,.T.);
#3654=ADVANCED_FACE('',(#707),#478,.T.);
#3655=ADVANCED_FACE('',(#708),#479,.T.);
#3656=ADVANCED_FACE('',(#709),#480,.T.);
#3657=ADVANCED_FACE('',(#710),#3440,.F.);
#3658=ADVANCED_FACE('',(#711),#481,.T.);
#3659=ADVANCED_FACE('',(#712),#482,.T.);
#3660=ADVANCED_FACE('',(#713),#483,.T.);
#3661=ADVANCED_FACE('',(#714,#353),#484,.T.);
#3662=ADVANCED_FACE('',(#715,#354),#485,.F.);
#3699=CLOSED_SHELL('',(#3652,#3653,#3654,#3655,#3656,#3657,#3658,#3659,
#3660,#3661,#3662));
#4372=AXIS2_PLACEMENT_3D('',#8215,#5462,#5463);
#4373=AXIS2_PLACEMENT_3D('',#8216,#5464,#5465);
#4374=AXIS2_PLACEMENT_3D('',#8228,#5467,#5468);
#4375=AXIS2_PLACEMENT_3D('',#8244,#5469,#5470);
#4376=AXIS2_PLACEMENT_3D('',#8246,#5471,#5472);
#4377=AXIS2_PLACEMENT_3D('',#8272,#5474,#5475);
#4378=AXIS2_PLACEMENT_3D('',#8275,#5478,#5479);
#4379=AXIS2_PLACEMENT_3D('',#8277,#5481,#5482);
#4380=AXIS2_PLACEMENT_3D('',#8279,#5484,#5485);
#4381=AXIS2_PLACEMENT_3D('',#8281,#5486,#5487);
#4382=AXIS2_PLACEMENT_3D('',#8284,#5489,#5490);
#4383=AXIS2_PLACEMENT_3D('',#8285,#5491,#5492);
#4384=AXIS2_PLACEMENT_3D('',#8287,#5494,#5495);
#4385=AXIS2_PLACEMENT_3D('',#8289,#5497,#5498);
#4386=AXIS2_PLACEMENT_3D('',#8290,#5499,#5500);
#4387=AXIS2_PLACEMENT_3D('',#8291,#5501,#5502);
#5462=DIRECTION('axis',(0.,0.,1.));
#5463=DIRECTION('refdir',(1.,0.,0.));
#5464=DIRECTION('center_axis',(0.,1.,0.));
#5465=DIRECTION('ref_axis',(1.,0.,0.));
#5466=DIRECTION('',(0.866025403784439,-0.5,1.06057523872491E-16));
#5467=DIRECTION('center_axis',(0.,-1.,0.));
#5468=DIRECTION('ref_axis',(1.,0.,0.));
#5469=DIRECTION('center_axis',(0.,-1.,0.));
#5470=DIRECTION('ref_axis',(1.,0.,0.));
#5471=DIRECTION('center_axis',(0.,1.,0.));
#5472=DIRECTION('ref_axis',(1.,0.,0.));
#5473=DIRECTION('',(-0.866025403784439,-0.5,-1.06057523872491E-16));
#5474=DIRECTION('center_axis',(1.4792020664489E-16,0.,-1.));
#5475=DIRECTION('ref_axis',(-1.,0.,-1.4792020664489E-16));
#5476=DIRECTION('',(0.,1.,0.));
#5477=DIRECTION('',(0.,1.,0.));
#5478=DIRECTION('center_axis',(-0.866025403784439,0.,-0.5));
#5479=DIRECTION('ref_axis',(-0.5,0.,0.866025403784439));
#5480=DIRECTION('',(0.,1.,0.));
#5481=DIRECTION('center_axis',(-0.866025403784439,0.,0.5));
#5482=DIRECTION('ref_axis',(0.5,0.,0.866025403784439));
#5483=DIRECTION('',(0.,1.,0.));
#5484=DIRECTION('center_axis',(0.,1.,0.));
#5485=DIRECTION('ref_axis',(1.,0.,0.));
#5486=DIRECTION('center_axis',(0.,1.,0.));
#5487=DIRECTION('ref_axis',(1.,0.,0.));
#5488=DIRECTION('',(0.,-1.,0.));
#5489=DIRECTION('center_axis',(0.,1.,0.));
#5490=DIRECTION('ref_axis',(1.,0.,0.));
#5491=DIRECTION('center_axis',(-2.95840413289779E-16,0.,1.));
#5492=DIRECTION('ref_axis',(1.,0.,2.95840413289779E-16));
#5493=DIRECTION('',(0.,1.,0.));
#5494=DIRECTION('center_axis',(0.866025403784439,0.,-0.5));
#5495=DIRECTION('ref_axis',(-0.5,0.,-0.866025403784439));
#5496=DIRECTION('',(0.,1.,0.));
#5497=DIRECTION('center_axis',(0.866025403784439,0.,0.5));
#5498=DIRECTION('ref_axis',(0.5,0.,-0.866025403784439));
#5499=DIRECTION('center_axis',(0.,1.,0.));
#5500=DIRECTION('ref_axis',(1.,0.,0.));
#5501=DIRECTION('center_axis',(0.,1.,0.));
#5502=DIRECTION('ref_axis',(1.,0.,0.));
#8215=CARTESIAN_POINT('',(0.,0.,0.));
#8216=CARTESIAN_POINT('Origin',(0.,0.067277284513851,0.));
#8217=CARTESIAN_POINT('',(-0.375277674973257,0.0768195421087395,0.65));
#8218=CARTESIAN_POINT('',(0.375277674973257,0.0768195421087395,0.65));
#8219=CARTESIAN_POINT('Ctrl Pts',(-0.375277674973257,0.0768195421087395,
0.65));
#8220=CARTESIAN_POINT('Ctrl Pts',(1.66533453693773E-13,-0.0315137912242439,
0.65));
#8221=CARTESIAN_POINT('Ctrl Pts',(0.375277674973257,0.0768195421087394,
0.65));
#8222=CARTESIAN_POINT('',(-0.750555349946514,0.0768195421087394,-9.19165206894919E-17));
#8223=CARTESIAN_POINT('Ctrl Pts',(-0.750555349946514,0.0768195421087394,
-9.19165206894919E-17));
#8224=CARTESIAN_POINT('Ctrl Pts',(-0.562916512459802,-0.0315137912242434,
0.325000000000144));
#8225=CARTESIAN_POINT('Ctrl Pts',(-0.375277674973257,0.0768195421087395,
0.65));
#8226=CARTESIAN_POINT('',(-0.6175,-2.77555756156289E-17,-7.5621939847349E-17));
#8227=CARTESIAN_POINT('',(-0.734027674973257,0.067277284513851,-8.98924642641573E-17));
#8228=CARTESIAN_POINT('Origin',(0.,0.,0.));
#8229=CARTESIAN_POINT('',(-0.375277674973257,0.0768195421087395,-0.65));
#8230=CARTESIAN_POINT('Ctrl Pts',(-0.375277674973257,0.0768195421087395,
-0.65));
#8231=CARTESIAN_POINT('Ctrl Pts',(-0.562916512459968,-0.0315137912242437,
-0.324999999999856));
#8232=CARTESIAN_POINT('Ctrl Pts',(-0.750555349946514,0.0768195421087395,
-9.19165206894919E-17));
#8233=CARTESIAN_POINT('',(0.375277674973257,0.0768195421087395,-0.65));
#8234=CARTESIAN_POINT('Ctrl Pts',(0.375277674973257,0.0768195421087395,
-0.65));
#8235=CARTESIAN_POINT('Ctrl Pts',(-1.66144875635155E-13,-0.0315137912242437,
-0.65));
#8236=CARTESIAN_POINT('Ctrl Pts',(-0.375277674973257,0.0768195421087395,
-0.65));
#8237=CARTESIAN_POINT('',(0.750555349946514,0.0768195421087394,0.));
#8238=CARTESIAN_POINT('Ctrl Pts',(0.750555349946514,0.0768195421087394,
0.));
#8239=CARTESIAN_POINT('Ctrl Pts',(0.562916512459802,-0.0315137912242436,
-0.325000000000144));
#8240=CARTESIAN_POINT('Ctrl Pts',(0.375277674973257,0.0768195421087395,
-0.65));
#8241=CARTESIAN_POINT('Ctrl Pts',(0.375277674973257,0.0768195421087394,
0.65));
#8242=CARTESIAN_POINT('Ctrl Pts',(0.562916512459968,-0.0315137912242439,
0.324999999999856));
#8243=CARTESIAN_POINT('Ctrl Pts',(0.750555349946514,0.0768195421087394,
0.));
#8244=CARTESIAN_POINT('Origin',(0.,0.612722715486149,0.));
#8245=CARTESIAN_POINT('',(-0.6175,0.68,-7.5621939847349E-17));
#8246=CARTESIAN_POINT('Origin',(0.,0.68,0.));
#8247=CARTESIAN_POINT('',(-0.750555349946514,0.603180457891261,-9.19165206894919E-17));
#8248=CARTESIAN_POINT('',(-0.734027674973257,0.612722715486149,-8.98924642641573E-17));
#8249=CARTESIAN_POINT('',(-0.375277674973257,0.603180457891261,0.65));
#8250=CARTESIAN_POINT('Ctrl Pts',(-0.375277674973257,0.603180457891261,
0.65));
#8251=CARTESIAN_POINT('Ctrl Pts',(-0.562916512459968,0.711513791224243,
0.324999999999856));
#8252=CARTESIAN_POINT('Ctrl Pts',(-0.750555349946514,0.603180457891261,
-9.19165206894919E-17));
#8253=CARTESIAN_POINT('',(0.375277674973257,0.603180457891261,0.65));
#8254=CARTESIAN_POINT('Ctrl Pts',(0.375277674973257,0.603180457891261,0.65));
#8255=CARTESIAN_POINT('Ctrl Pts',(-1.66755498298699E-13,0.711513791224244,
0.65));
#8256=CARTESIAN_POINT('Ctrl Pts',(-0.375277674973257,0.603180457891261,
0.65));
#8257=CARTESIAN_POINT('',(0.750555349946514,0.603180457891261,0.));
#8258=CARTESIAN_POINT('Ctrl Pts',(0.750555349946514,0.603180457891261,0.));
#8259=CARTESIAN_POINT('Ctrl Pts',(0.562916512459802,0.711513791224244,0.325000000000144));
#8260=CARTESIAN_POINT('Ctrl Pts',(0.375277674973257,0.603180457891261,0.65));
#8261=CARTESIAN_POINT('',(0.375277674973257,0.603180457891261,-0.65));
#8262=CARTESIAN_POINT('Ctrl Pts',(0.375277674973257,0.603180457891261,-0.65));
#8263=CARTESIAN_POINT('Ctrl Pts',(0.562916512459969,0.711513791224244,-0.324999999999856));
#8264=CARTESIAN_POINT('Ctrl Pts',(0.750555349946514,0.603180457891261,0.));
#8265=CARTESIAN_POINT('',(-0.375277674973257,0.603180457891261,-0.65));
#8266=CARTESIAN_POINT('Ctrl Pts',(-0.375277674973257,0.603180457891261,
-0.65));
#8267=CARTESIAN_POINT('Ctrl Pts',(1.66422431391311E-13,0.711513791224244,
-0.65));
#8268=CARTESIAN_POINT('Ctrl Pts',(0.375277674973257,0.603180457891261,-0.65));
#8269=CARTESIAN_POINT('Ctrl Pts',(-0.750555349946514,0.603180457891261,
-9.19165206894919E-17));
#8270=CARTESIAN_POINT('Ctrl Pts',(-0.562916512459802,0.711513791224244,
-0.325000000000144));
#8271=CARTESIAN_POINT('Ctrl Pts',(-0.375277674973257,0.603180457891261,
-0.65));
#8272=CARTESIAN_POINT('Origin',(0.375277674973257,0.,-0.65));
#8273=CARTESIAN_POINT('',(-0.375277674973257,0.,-0.65));
#8274=CARTESIAN_POINT('',(0.375277674973257,0.,-0.65));
#8275=CARTESIAN_POINT('Origin',(-0.375277674973257,0.,-0.65));
#8276=CARTESIAN_POINT('',(-0.750555349946514,0.,-9.19165206894919E-17));
#8277=CARTESIAN_POINT('Origin',(-0.750555349946514,0.,-9.19165206894919E-17));
#8278=CARTESIAN_POINT('',(-0.375277674973257,0.,0.65));
#8279=CARTESIAN_POINT('Origin',(0.,0.,0.));
#8280=CARTESIAN_POINT('',(-0.338975,0.68,4.15124648740974E-17));
#8281=CARTESIAN_POINT('Origin',(0.,0.68,0.));
#8282=CARTESIAN_POINT('',(-0.338975,0.,4.15124648740974E-17));
#8283=CARTESIAN_POINT('',(-0.338975,0.,4.15124648740974E-17));
#8284=CARTESIAN_POINT('Origin',(0.,0.,0.));
#8285=CARTESIAN_POINT('Origin',(-0.375277674973257,0.,0.65));
#8286=CARTESIAN_POINT('',(0.375277674973257,0.,0.65));
#8287=CARTESIAN_POINT('Origin',(0.750555349946514,0.,0.));
#8288=CARTESIAN_POINT('',(0.750555349946514,0.,0.));
#8289=CARTESIAN_POINT('Origin',(0.375277674973257,0.,0.65));
#8290=CARTESIAN_POINT('Origin',(0.,0.68,-1.11022302462516E-16));
#8291=CARTESIAN_POINT('Origin',(0.,0.,-1.11022302462516E-16));
#8400=UNCERTAINTY_MEASURE_WITH_UNIT(LENGTH_MEASURE(0.001),#8429,
'DISTANCE_ACCURACY_VALUE',
'Maximum model space distance between geometric entities at asserted c
onnectivities');
#8402=UNCERTAINTY_MEASURE_WITH_UNIT(LENGTH_MEASURE(0.001),#8429,
'DISTANCE_ACCURACY_VALUE',
'Maximum model space distance between geometric entities at asserted c
onnectivities');
#8426=(
GEOMETRIC_REPRESENTATION_CONTEXT(3)
GLOBAL_UNCERTAINTY_ASSIGNED_CONTEXT((#8400))
GLOBAL_UNIT_ASSIGNED_CONTEXT((#8429,#8431,#8432))
REPRESENTATION_CONTEXT('','3D')
);
#8428=(
GEOMETRIC_REPRESENTATION_CONTEXT(3)
GLOBAL_UNCERTAINTY_ASSIGNED_CONTEXT((#8402))
GLOBAL_UNIT_ASSIGNED_CONTEXT((#8429,#8431,#8432))
REPRESENTATION_CONTEXT('','3D')
);
#8429=(
LENGTH_UNIT()
NAMED_UNIT(*)
SI_UNIT(.CENTI.,.METRE.)
);
#8431=(
NAMED_UNIT(*)
PLANE_ANGLE_UNIT()
SI_UNIT($,.RADIAN.)
);
#8432=(
NAMED_UNIT(*)
SI_UNIT($,.STERADIAN.)
SOLID_ANGLE_UNIT()
);
#8456=SHAPE_DEFINITION_REPRESENTATION(#8481,#8537);
#8481=PRODUCT_DEFINITION_SHAPE('',$,#8563);
#8537=SHAPE_REPRESENTATION('',(#4372),#8426);
#8539=PRODUCT_DEFINITION_CONTEXT('part definition',#8616,'design');
#8563=PRODUCT_DEFINITION('Hex Nut - M8','Hex Nut - M8',#8588,
#8539);
#8588=PRODUCT_DEFINITION_FORMATION('',$,#8641);
#8616=APPLICATION_CONTEXT(
'Core Data for Automotive Mechanical Design Process');
#8617=PRODUCT_CONTEXT('part definition',#8616,'mechanical');
#8641=PRODUCT('Hex Nut - M8','Hex Nut - M8','Hex Nut - M8',
(#8617));
#8706=COLOUR_RGB('Black',0.12,0.14,0.17);
#8707=FILL_AREA_STYLE_COLOUR('',#8706);
#8708=FILL_AREA_STYLE('',(#8707));
#8709=SURFACE_STYLE_FILL_AREA(#8708);
#8710=SURFACE_SIDE_STYLE('',(#8709));
#8711=SURFACE_STYLE_USAGE(.BOTH.,#8710);
#8712=PRESENTATION_STYLE_ASSIGNMENT((#8711));
ENDSEC;
END-ISO-10303-21;
